ISO-10303-21;
HEADER;
FILE_DESCRIPTION((''),'2;1');
FILE_NAME('HUB_LOCK_WASHER.step','2026-10-01T22:05:39-07:00',(''),(''),'','','');
FILE_SCHEMA (('AUTOMOTIVE_DESIGN { 1 0 10303 214 3 1 1 }'));
ENDSEC;
DATA;
#10=MECHANICAL_DESIGN_GEOMETRIC_PRESENTATION_REPRESENTATION('',(#642),#24628);
#558=SHAPE_REPRESENTATION_RELATIONSHIP('SRR','None',#24833,#600) ;
#600=ADVANCED_BREP_SHAPE_REPRESENTATION('',(#681),#24623) ;
#642=STYLED_ITEM('',(#25030),#681) ;
#681=MANIFOLD_SOLID_BREP('HUB_LOCK_WASHER',#13184) ;
#943=FACE_BOUND('',#4704,.T.) ;
#944=FACE_BOUND('',#4706,.T.) ;
#1759=LINE('',#24318,#2595) ;
#1760=LINE('',#24324,#2596) ;
#2595=VECTOR('',#19466,0.525) ;
#2596=VECTOR('',#19473,1.) ;
#2946=CYLINDRICAL_SURFACE('',#15309,0.525) ;
#2947=CYLINDRICAL_SURFACE('',#15312,1.) ;
#3677=FACE_OUTER_BOUND('',#4701,.T.) ;
#3678=FACE_OUTER_BOUND('',#4702,.T.) ;
#3679=FACE_OUTER_BOUND('',#4703,.T.) ;
#3680=FACE_OUTER_BOUND('',#4705,.T.) ;
#4701=EDGE_LOOP('',(#11815,#11816,#11817,#11818)) ;
#4702=EDGE_LOOP('',(#11819,#11820,#11821,#11822)) ;
#4703=EDGE_LOOP('',(#11823)) ;
#4704=EDGE_LOOP('',(#11824)) ;
#4705=EDGE_LOOP('',(#11825)) ;
#4706=EDGE_LOOP('',(#11826)) ;
#5525=CIRCLE('',#15310,0.525) ;
#5526=CIRCLE('',#15311,0.525) ;
#5527=CIRCLE('',#15313,1.) ;
#5528=CIRCLE('',#15314,1.) ;
#6673=VERTEX_POINT('',#24315) ;
#6674=VERTEX_POINT('',#24317) ;
#6675=VERTEX_POINT('',#24321) ;
#6676=VERTEX_POINT('',#24323) ;
#8397=EDGE_CURVE('',#6673,#6673,#5525,.T.) ;
#8398=EDGE_CURVE('',#6673,#6674,#1759,.T.) ;
#8399=EDGE_CURVE('',#6674,#6674,#5526,.T.) ;
#8400=EDGE_CURVE('',#6675,#6675,#5527,.T.) ;
#8401=EDGE_CURVE('',#6675,#6676,#1760,.T.) ;
#8402=EDGE_CURVE('',#6676,#6676,#5528,.T.) ;
#11815=ORIENTED_EDGE('',*,*,#8397,.F.) ;
#11816=ORIENTED_EDGE('',*,*,#8398,.T.) ;
#11817=ORIENTED_EDGE('',*,*,#8399,.F.) ;
#11818=ORIENTED_EDGE('',*,*,#8398,.F.) ;
#11819=ORIENTED_EDGE('',*,*,#8400,.F.) ;
#11820=ORIENTED_EDGE('',*,*,#8401,.T.) ;
#11821=ORIENTED_EDGE('',*,*,#8402,.F.) ;
#11822=ORIENTED_EDGE('',*,*,#8401,.F.) ;
#11823=ORIENTED_EDGE('',*,*,#8402,.T.) ;
#11824=ORIENTED_EDGE('',*,*,#8397,.T.) ;
#11825=ORIENTED_EDGE('',*,*,#8400,.T.) ;
#11826=ORIENTED_EDGE('',*,*,#8399,.T.) ;
#12311=PLANE('',#15315) ;
#12312=PLANE('',#15316) ;
#13072=ADVANCED_FACE('',(#3677),#2946,.F.) ;
#13073=ADVANCED_FACE('',(#3678),#2947,.T.) ;
#13074=ADVANCED_FACE('',(#3679,#943),#12311,.T.) ;
#13075=ADVANCED_FACE('',(#3680,#944),#12312,.T.) ;
#13184=CLOSED_SHELL('',(#13072,#13073,#13074,#13075)) ;
#15308=AXIS2_PLACEMENT_3D('',#24313,#19460,#19461) ;
#15309=AXIS2_PLACEMENT_3D('',#24314,#19462,#19463) ;
#15310=AXIS2_PLACEMENT_3D('',#24316,#19464,#19465) ;
#15311=AXIS2_PLACEMENT_3D('',#24319,#19467,#19468) ;
#15312=AXIS2_PLACEMENT_3D('',#24320,#19469,#19470) ;
#15313=AXIS2_PLACEMENT_3D('',#24322,#19471,#19472) ;
#15314=AXIS2_PLACEMENT_3D('',#24325,#19474,#19475) ;
#15315=AXIS2_PLACEMENT_3D('',#24326,#19476,#19477) ;
#15316=AXIS2_PLACEMENT_3D('',#24327,#19478,#19479) ;
#19460=DIRECTION('axis',(0.,0.,1.)) ;
#19461=DIRECTION('refdir',(1.,0.,0.)) ;
#19462=DIRECTION('center_axis',(0.,1.,0.)) ;
#19463=DIRECTION('ref_axis',(1.,0.,0.)) ;
#19464=DIRECTION('center_axis',(0.,1.,0.)) ;
#19465=DIRECTION('ref_axis',(1.,0.,0.)) ;
#19466=DIRECTION('',(0.,1.,0.)) ;
#19467=DIRECTION('center_axis',(0.,-1.,0.)) ;
#19468=DIRECTION('ref_axis',(1.,0.,0.)) ;
#19469=DIRECTION('center_axis',(0.,1.,0.)) ;
#19470=DIRECTION('ref_axis',(1.,0.,0.)) ;
#19471=DIRECTION('center_axis',(0.,1.,0.)) ;
#19472=DIRECTION('ref_axis',(1.,0.,0.)) ;
#19473=DIRECTION('',(0.,-1.,0.)) ;
#19474=DIRECTION('center_axis',(0.,-1.,0.)) ;
#19475=DIRECTION('ref_axis',(1.,0.,0.)) ;
#19476=DIRECTION('center_axis',(0.,-1.,0.)) ;
#19477=DIRECTION('ref_axis',(-1.,0.,0.)) ;
#19478=DIRECTION('center_axis',(0.,1.,0.)) ;
#19479=DIRECTION('ref_axis',(1.,0.,0.)) ;
#24313=CARTESIAN_POINT('',(0.,0.,0.)) ;
#24314=CARTESIAN_POINT('Origin',(0.,-0.2,0.)) ;
#24315=CARTESIAN_POINT('',(-0.525,-0.3,6.4293956955236E-17)) ;
#24316=CARTESIAN_POINT('Origin',(0.,-0.3,0.)) ;
#24317=CARTESIAN_POINT('',(-0.525,-0.1,-6.4293956955236E-17)) ;
#24318=CARTESIAN_POINT('',(-0.525,-0.2,6.4293956955236E-17)) ;
#24319=CARTESIAN_POINT('Origin',(0.,-0.1,0.)) ;
#24320=CARTESIAN_POINT('Origin',(0.,-0.2,0.)) ;
#24321=CARTESIAN_POINT('',(-1.,-0.1,1.22464679914735E-16)) ;
#24322=CARTESIAN_POINT('Origin',(0.,-0.1,0.)) ;
#24323=CARTESIAN_POINT('',(-1.,-0.3,1.22464679914735E-16)) ;
#24324=CARTESIAN_POINT('',(-1.,-0.2,1.22464679914735E-16)) ;
#24325=CARTESIAN_POINT('Origin',(0.,-0.3,0.)) ;
#24326=CARTESIAN_POINT('Origin',(0.,-0.3,0.)) ;
#24327=CARTESIAN_POINT('Origin',(0.,-0.1,0.)) ;
#24575=UNCERTAINTY_MEASURE_WITH_UNIT(LENGTH_MEASURE(0.001),#24629,
'DISTANCE_ACCURACY_VALUE',
'Maximum model space distance between geometric entities at asserted c
onnectivities') ;
#24580=UNCERTAINTY_MEASURE_WITH_UNIT(LENGTH_MEASURE(0.001),#24629,
'DISTANCE_ACCURACY_VALUE',
'Maximum model space distance between geometric entities at asserted c
onnectivities') ;
#24623=(
GEOMETRIC_REPRESENTATION_CONTEXT(3)
GLOBAL_UNCERTAINTY_ASSIGNED_CONTEXT((#24575))
GLOBAL_UNIT_ASSIGNED_CONTEXT((#24629,#24631,#24632))
REPRESENTATION_CONTEXT('','3D')
) ;
#24628=(
GEOMETRIC_REPRESENTATION_CONTEXT(3)
GLOBAL_UNCERTAINTY_ASSIGNED_CONTEXT((#24580))
GLOBAL_UNIT_ASSIGNED_CONTEXT((#24629,#24631,#24632))
REPRESENTATION_CONTEXT('','3D')
) ;
#24629=(
LENGTH_UNIT()
NAMED_UNIT(*)
SI_UNIT(.CENTI.,.METRE.)
) ;
#24631=(
NAMED_UNIT(*)
PLANE_ANGLE_UNIT()
SI_UNIT($,.RADIAN.)
) ;
#24632=(
NAMED_UNIT(*)
SI_UNIT($,.STERADIAN.)
SOLID_ANGLE_UNIT()
) ;
#24675=SHAPE_DEFINITION_REPRESENTATION(#24763,#24833) ;
#24763=PRODUCT_DEFINITION_SHAPE('',$,#24881) ;
#24833=SHAPE_REPRESENTATION('',(#15308),#24623) ;
#24838=PRODUCT_DEFINITION_CONTEXT('part definition',#24981,'design') ;
#24881=PRODUCT_DEFINITION('HUB_LOCK_WASHER','HUB_LOCK_WASHER',#24928,
#24838) ;
#24928=PRODUCT_DEFINITION_FORMATION('',$,#25025) ;
#24981=APPLICATION_CONTEXT(
'Core Data for Automotive Mechanical Design Process') ;
#24982=PRODUCT_CONTEXT('part definition',#24981,'mechanical') ;
#25025=PRODUCT('HUB_LOCK_WASHER','HUB_LOCK_WASHER',$,(#24982)) ;
#25030=PRESENTATION_STYLE_ASSIGNMENT((#25040)) ;
#25040=SURFACE_STYLE_USAGE(.BOTH.,#25050) ;
#25050=SURFACE_SIDE_STYLE('',(#25060)) ;
#25060=SURFACE_STYLE_FILL_AREA(#25070) ;
#25070=FILL_AREA_STYLE('Steel - Satin',(#25080)) ;
#25080=FILL_AREA_STYLE_COLOUR('Steel - Satin',#25090) ;
#25090=COLOUR_RGB('Steel - Satin', 0.66274510, 0.83137255, 0.94901961) ;
ENDSEC;
END-ISO-10303-21;
